ISO-10303-21;
HEADER;
/* Generated by software containing ST-Developer
 * from STEP Tools, Inc. (www.steptools.com) 
 */

FILE_DESCRIPTION(
/* description */ (''),
/* implementation_level */ '2;1');

FILE_NAME(
/* name */ '14_Case_Drain_Plug_9-16-18.step',
/* time_stamp */ '2026-10-26T06:59:52-07:00',
/* author */ (''),
/* organization */ (''),
/* preprocessor_version */ 'ST-DEVELOPER v20.2',
/* originating_system */ 'Autodesk Translation Framework v15.15.0.0',
/* authorisation */ '');

FILE_SCHEMA (('AUTOMOTIVE_DESIGN { 1 0 10303 214 3 1 1 }'));
ENDSEC;

DATA;
#10=MECHANICAL_DESIGN_GEOMETRIC_PRESENTATION_REPRESENTATION('',(#174),#46395);
#123=(
BOUNDED_CURVE()
B_SPLINE_CURVE(2,(#40519,#40520,#40521),.UNSPECIFIED.,.F.,.F.)
B_SPLINE_CURVE_WITH_KNOTS((3,3),(0.179912787003236,0.267754473851814),
 .UNSPECIFIED.)
CURVE()
GEOMETRIC_REPRESENTATION_ITEM()
RATIONAL_B_SPLINE_CURVE((1.0121972483025,1.01317411304726,1.0121972483025))
REPRESENTATION_ITEM('')
);
#124=(
BOUNDED_CURVE()
B_SPLINE_CURVE(2,(#40530,#40531,#40532),.UNSPECIFIED.,.F.,.F.)
B_SPLINE_CURVE_WITH_KNOTS((3,3),(0.179912787003235,0.267754473851812),
 .UNSPECIFIED.)
CURVE()
GEOMETRIC_REPRESENTATION_ITEM()
RATIONAL_B_SPLINE_CURVE((1.01219724830249,1.01317411304725,1.01219724830249))
REPRESENTATION_ITEM('')
);
#125=(
BOUNDED_CURVE()
B_SPLINE_CURVE(2,(#40538,#40539,#40540),.UNSPECIFIED.,.F.,.F.)
B_SPLINE_CURVE_WITH_KNOTS((3,3),(0.179912787003235,0.267754473851814),
 .UNSPECIFIED.)
CURVE()
GEOMETRIC_REPRESENTATION_ITEM()
RATIONAL_B_SPLINE_CURVE((1.01219724830251,1.01317411304727,1.01219724830251))
REPRESENTATION_ITEM('')
);
#126=(
BOUNDED_CURVE()
B_SPLINE_CURVE(2,(#40549,#40550,#40551),.UNSPECIFIED.,.F.,.F.)
B_SPLINE_CURVE_WITH_KNOTS((3,3),(0.179912787003232,0.267754473851811),
 .UNSPECIFIED.)
CURVE()
GEOMETRIC_REPRESENTATION_ITEM()
RATIONAL_B_SPLINE_CURVE((1.0121972483025,1.01317411304727,1.0121972483025))
REPRESENTATION_ITEM('')
);
#127=(
BOUNDED_CURVE()
B_SPLINE_CURVE(2,(#40557,#40558,#40559),.UNSPECIFIED.,.F.,.F.)
B_SPLINE_CURVE_WITH_KNOTS((3,3),(0.179912787003235,0.267754473851813),
 .UNSPECIFIED.)
CURVE()
GEOMETRIC_REPRESENTATION_ITEM()
RATIONAL_B_SPLINE_CURVE((1.0121972483025,1.01317411304727,1.0121972483025))
REPRESENTATION_ITEM('')
);
#128=(
BOUNDED_CURVE()
B_SPLINE_CURVE(2,(#40568,#40569,#40570),.UNSPECIFIED.,.F.,.F.)
B_SPLINE_CURVE_WITH_KNOTS((3,3),(0.179912787003235,0.267754473851813),
 .UNSPECIFIED.)
CURVE()
GEOMETRIC_REPRESENTATION_ITEM()
RATIONAL_B_SPLINE_CURVE((1.0121972483025,1.01317411304726,1.0121972483025))
REPRESENTATION_ITEM('')
);
#129=(
BOUNDED_CURVE()
B_SPLINE_CURVE(2,(#40574,#40575,#40576),.UNSPECIFIED.,.F.,.F.)
B_SPLINE_CURVE_WITH_KNOTS((3,3),(0.111302637204007,1.06697395554892),
 .UNSPECIFIED.)
CURVE()
GEOMETRIC_REPRESENTATION_ITEM()
RATIONAL_B_SPLINE_CURVE((1.03421564758363,1.16578435241637,1.03421564758363))
REPRESENTATION_ITEM('')
);
#130=(
BOUNDED_CURVE()
B_SPLINE_CURVE(2,(#40579,#40580,#40581),.UNSPECIFIED.,.F.,.F.)
B_SPLINE_CURVE_WITH_KNOTS((3,3),(0.111302637204007,0.589138296376461),
 .UNSPECIFIED.)
CURVE()
GEOMETRIC_REPRESENTATION_ITEM()
RATIONAL_B_SPLINE_CURVE((1.03421564758363,1.1,1.1))
REPRESENTATION_ITEM('')
);
#131=(
BOUNDED_CURVE()
B_SPLINE_CURVE(2,(#40582,#40583,#40584),.UNSPECIFIED.,.F.,.F.)
B_SPLINE_CURVE_WITH_KNOTS((3,3),(0.589138296376461,1.06697395554892),
 .UNSPECIFIED.)
CURVE()
GEOMETRIC_REPRESENTATION_ITEM()
RATIONAL_B_SPLINE_CURVE((1.1,1.1,1.03421564758363))
REPRESENTATION_ITEM('')
);
#132=(
BOUNDED_CURVE()
B_SPLINE_CURVE(2,(#40586,#40587,#40588),.UNSPECIFIED.,.F.,.F.)
B_SPLINE_CURVE_WITH_KNOTS((3,3),(0.111302637204006,1.06697395554891),
 .UNSPECIFIED.)
CURVE()
GEOMETRIC_REPRESENTATION_ITEM()
RATIONAL_B_SPLINE_CURVE((1.03421564758363,1.16578435241637,1.03421564758363))
REPRESENTATION_ITEM('')
);
#133=(
BOUNDED_CURVE()
B_SPLINE_CURVE(2,(#40658,#40659,#40660),.UNSPECIFIED.,.F.,.F.)
B_SPLINE_CURVE_WITH_KNOTS((3,3),(0.111302637204007,1.06697395554892),
 .UNSPECIFIED.)
CURVE()
GEOMETRIC_REPRESENTATION_ITEM()
RATIONAL_B_SPLINE_CURVE((1.03421564758363,1.16578435241637,1.03421564758363))
REPRESENTATION_ITEM('')
);
#134=(
BOUNDED_CURVE()
B_SPLINE_CURVE(2,(#40661,#40662,#40663),.UNSPECIFIED.,.F.,.F.)
B_SPLINE_CURVE_WITH_KNOTS((3,3),(0.111302637204007,1.06697395554892),
 .UNSPECIFIED.)
CURVE()
GEOMETRIC_REPRESENTATION_ITEM()
RATIONAL_B_SPLINE_CURVE((1.03421564758363,1.16578435241637,1.03421564758363))
REPRESENTATION_ITEM('')
);
#135=(
BOUNDED_CURVE()
B_SPLINE_CURVE(2,(#40664,#40665,#40666),.UNSPECIFIED.,.F.,.F.)
B_SPLINE_CURVE_WITH_KNOTS((3,3),(0.111302637204006,1.06697395554892),
 .UNSPECIFIED.)
CURVE()
GEOMETRIC_REPRESENTATION_ITEM()
RATIONAL_B_SPLINE_CURVE((1.03421564758363,1.16578435241637,1.03421564758363))
REPRESENTATION_ITEM('')
);
#146=SHAPE_REPRESENTATION_RELATIONSHIP('SRR','None',#46466,#160);
#160=ADVANCED_BREP_SHAPE_REPRESENTATION('',(#188),#46391);
#174=STYLED_ITEM('',(#46589),#188);
#188=MANIFOLD_SOLID_BREP('Body1',#24947);
#532=CYLINDRICAL_SURFACE('',#26575,7.14);
#533=CYLINDRICAL_SURFACE('',#26579,6.2);
#665=FACE_BOUND('',#4242,.T.);
#666=FACE_BOUND('',#4253,.T.);
#667=FACE_BOUND('',#4266,.T.);
#1542=PLANE('',#26529);
#1543=PLANE('',#26530);
#1544=PLANE('',#26531);
#1545=PLANE('',#26532);
#1546=PLANE('',#26533);
#1547=PLANE('',#26534);
#1548=PLANE('',#26535);
#1549=PLANE('',#26536);
#1550=PLANE('',#26537);
#1551=PLANE('',#26538);
#1552=PLANE('',#26539);
#1553=PLANE('',#26540);
#1554=PLANE('',#26541);
#1555=PLANE('',#26542);
#1556=PLANE('',#26543);
#1557=PLANE('',#26544);
#1558=PLANE('',#26545);
#1559=PLANE('',#26546);
#1560=PLANE('',#26547);
#1561=PLANE('',#26548);
#1562=PLANE('',#26549);
#1563=PLANE('',#26550);
#1564=PLANE('',#26552);
#1565=PLANE('',#26553);
#1566=PLANE('',#26554);
#1567=PLANE('',#26555);
#1568=PLANE('',#26556);
#1569=PLANE('',#26557);
#1570=PLANE('',#26558);
#1571=PLANE('',#26559);
#1572=PLANE('',#26560);
#1573=PLANE('',#26561);
#1574=PLANE('',#26563);
#1575=PLANE('',#26564);
#1576=PLANE('',#26565);
#1577=PLANE('',#26566);
#1578=PLANE('',#26568);
#1579=PLANE('',#26569);
#1580=PLANE('',#26570);
#1581=PLANE('',#26571);
#1582=PLANE('',#26577);
#2810=FACE_OUTER_BOUND('',#4220,.T.);
#2811=FACE_OUTER_BOUND('',#4221,.T.);
#2812=FACE_OUTER_BOUND('',#4222,.T.);
#2813=FACE_OUTER_BOUND('',#4223,.T.);
#2814=FACE_OUTER_BOUND('',#4224,.T.);
#2815=FACE_OUTER_BOUND('',#4225,.T.);
#2816=FACE_OUTER_BOUND('',#4226,.T.);
#2817=FACE_OUTER_BOUND('',#4227,.T.);
#2818=FACE_OUTER_BOUND('',#4228,.T.);
#2819=FACE_OUTER_BOUND('',#4229,.T.);
#2820=FACE_OUTER_BOUND('',#4230,.T.);
#2821=FACE_OUTER_BOUND('',#4231,.T.);
#2822=FACE_OUTER_BOUND('',#4232,.T.);
#2823=FACE_OUTER_BOUND('',#4233,.T.);
#2824=FACE_OUTER_BOUND('',#4234,.T.);
#2825=FACE_OUTER_BOUND('',#4235,.T.);
#2826=FACE_OUTER_BOUND('',#4236,.T.);
#2827=FACE_OUTER_BOUND('',#4237,.T.);
#2828=FACE_OUTER_BOUND('',#4238,.T.);
#2829=FACE_OUTER_BOUND('',#4239,.T.);
#2830=FACE_OUTER_BOUND('',#4240,.T.);
#2831=FACE_OUTER_BOUND('',#4241,.T.);
#2832=FACE_OUTER_BOUND('',#4243,.T.);
#2833=FACE_OUTER_BOUND('',#4244,.T.);
#2834=FACE_OUTER_BOUND('',#4245,.T.);
#2835=FACE_OUTER_BOUND('',#4246,.T.);
#2836=FACE_OUTER_BOUND('',#4247,.T.);
#2837=FACE_OUTER_BOUND('',#4248,.T.);
#2838=FACE_OUTER_BOUND('',#4249,.T.);
#2839=FACE_OUTER_BOUND('',#4250,.T.);
#2840=FACE_OUTER_BOUND('',#4251,.T.);
#2841=FACE_OUTER_BOUND('',#4252,.T.);
#2842=FACE_OUTER_BOUND('',#4254,.T.);
#2843=FACE_OUTER_BOUND('',#4255,.T.);
#2844=FACE_OUTER_BOUND('',#4256,.T.);
#2845=FACE_OUTER_BOUND('',#4257,.T.);
#2846=FACE_OUTER_BOUND('',#4258,.T.);
#2847=FACE_OUTER_BOUND('',#4259,.T.);
#2848=FACE_OUTER_BOUND('',#4260,.T.);
#2849=FACE_OUTER_BOUND('',#4261,.T.);
#2850=FACE_OUTER_BOUND('',#4262,.T.);
#2851=FACE_OUTER_BOUND('',#4263,.T.);
#2852=FACE_OUTER_BOUND('',#4264,.T.);
#2853=FACE_OUTER_BOUND('',#4265,.T.);
#2854=FACE_OUTER_BOUND('',#4267,.T.);
#4220=EDGE_LOOP('',(#22322,#22323,#22324));
#4221=EDGE_LOOP('',(#22325,#22326,#22327));
#4222=EDGE_LOOP('',(#22328,#22329,#22330));
#4223=EDGE_LOOP('',(#22331,#22332,#22333));
#4224=EDGE_LOOP('',(#22334,#22335,#22336,#22337));
#4225=EDGE_LOOP('',(#22338,#22339,#22340));
#4226=EDGE_LOOP('',(#22341,#22342,#22343));
#4227=EDGE_LOOP('',(#22344,#22345,#22346,#22347));
#4228=EDGE_LOOP('',(#22348,#22349,#22350,#22351));
#4229=EDGE_LOOP('',(#22352,#22353,#22354,#22355));
#4230=EDGE_LOOP('',(#22356,#22357,#22358,#22359));
#4231=EDGE_LOOP('',(#22360,#22361,#22362,#22363));
#4232=EDGE_LOOP('',(#22364,#22365,#22366,#22367));
#4233=EDGE_LOOP('',(#22368,#22369,#22370,#22371));
#4234=EDGE_LOOP('',(#22372,#22373,#22374,#22375));
#4235=EDGE_LOOP('',(#22376,#22377,#22378,#22379));
#4236=EDGE_LOOP('',(#22380,#22381,#22382,#22383));
#4237=EDGE_LOOP('',(#22384,#22385,#22386,#22387));
#4238=EDGE_LOOP('',(#22388,#22389,#22390,#22391));
#4239=EDGE_LOOP('',(#22392,#22393,#22394,#22395,#22396));
#4240=EDGE_LOOP('',(#22397,#22398,#22399,#22400));
#4241=EDGE_LOOP('',(#22401,#22402,#22403,#22404,#22405,#22406));
#4242=EDGE_LOOP('',(#22407));
#4243=EDGE_LOOP('',(#22408,#22409,#22410,#22411));
#4244=EDGE_LOOP('',(#22412,#22413,#22414,#22415));
#4245=EDGE_LOOP('',(#22416,#22417,#22418,#22419));
#4246=EDGE_LOOP('',(#22420,#22421,#22422,#22423));
#4247=EDGE_LOOP('',(#22424,#22425,#22426,#22427));
#4248=EDGE_LOOP('',(#22428,#22429,#22430,#22431));
#4249=EDGE_LOOP('',(#22432,#22433,#22434,#22435));
#4250=EDGE_LOOP('',(#22436,#22437,#22438,#22439));
#4251=EDGE_LOOP('',(#22440,#22441,#22442,#22443));
#4252=EDGE_LOOP('',(#22444));
#4253=EDGE_LOOP('',(#22445,#22446,#22447,#22448,#22449,#22450));
#4254=EDGE_LOOP('',(#22451,#22452,#22453,#22454));
#4255=EDGE_LOOP('',(#22455,#22456,#22457,#22458));
#4256=EDGE_LOOP('',(#22459,#22460,#22461,#22462));
#4257=EDGE_LOOP('',(#22463,#22464,#22465,#22466,#22467,#22468));
#4258=EDGE_LOOP('',(#22469,#22470,#22471,#22472,#22473,#22474,#22475,#22476,
#22477,#22478,#22479,#22480,#22481,#22482,#22483,#22484));
#4259=EDGE_LOOP('',(#22485,#22486,#22487,#22488));
#4260=EDGE_LOOP('',(#22489,#22490,#22491,#22492));
#4261=EDGE_LOOP('',(#22493,#22494,#22495,#22496));
#4262=EDGE_LOOP('',(#22497));
#4263=EDGE_LOOP('',(#22498,#22499,#22500,#22501));
#4264=EDGE_LOOP('',(#22502,#22503,#22504,#22505));
#4265=EDGE_LOOP('',(#22506));
#4266=EDGE_LOOP('',(#22507));
#4267=EDGE_LOOP('',(#22508,#22509,#22510,#22511));
#7001=LINE('',#40468,#9870);
#7002=LINE('',#40470,#9871);
#7003=LINE('',#40471,#9872);
#7004=LINE('',#40475,#9873);
#7005=LINE('',#40477,#9874);
#7006=LINE('',#40478,#9875);
#7007=LINE('',#40482,#9876);
#7008=LINE('',#40484,#9877);
#7009=LINE('',#40485,#9878);
#7010=LINE('',#40489,#9879);
#7011=LINE('',#40491,#9880);
#7012=LINE('',#40492,#9881);
#7013=LINE('',#40494,#9882);
#7014=LINE('',#40495,#9883);
#7015=LINE('',#40499,#9884);
#7016=LINE('',#40501,#9885);
#7017=LINE('',#40502,#9886);
#7018=LINE('',#40506,#9887);
#7019=LINE('',#40508,#9888);
#7020=LINE('',#40509,#9889);
#7021=LINE('',#40511,#9890);
#7022=LINE('',#40512,#9891);
#7023=LINE('',#40514,#9892);
#7024=LINE('',#40515,#9893);
#7025=LINE('',#40522,#9894);
#7026=LINE('',#40523,#9895);
#7027=LINE('',#40525,#9896);
#7028=LINE('',#40526,#9897);
#7029=LINE('',#40533,#9898);
#7030=LINE('',#40534,#9899);
#7031=LINE('',#40541,#9900);
#7032=LINE('',#40542,#9901);
#7033=LINE('',#40544,#9902);
#7034=LINE('',#40545,#9903);
#7035=LINE('',#40552,#9904);
#7036=LINE('',#40553,#9905);
#7037=LINE('',#40560,#9906);
#7038=LINE('',#40561,#9907);
#7039=LINE('',#40563,#9908);
#7040=LINE('',#40564,#9909);
#7041=LINE('',#40571,#9910);
#7042=LINE('',#40572,#9911);
#7043=LINE('',#40595,#9912);
#7044=LINE('',#40597,#9913);
#7045=LINE('',#40599,#9914);
#7046=LINE('',#40600,#9915);
#7047=LINE('',#40603,#9916);
#7048=LINE('',#40605,#9917);
#7049=LINE('',#40606,#9918);
#7050=LINE('',#40610,#9919);
#7051=LINE('',#40612,#9920);
#7052=LINE('',#40614,#9921);
#7053=LINE('',#40615,#9922);
#7054=LINE('',#40618,#9923);
#7055=LINE('',#40620,#9924);
#7056=LINE('',#40621,#9925);
#7057=LINE('',#40623,#9926);
#7058=LINE('',#40624,#9927);
#7059=LINE('',#40626,#9928);
#7060=LINE('',#40627,#9929);
#7061=LINE('',#40630,#9930);
#7062=LINE('',#40632,#9931);
#7063=LINE('',#40633,#9932);
#7064=LINE('',#40636,#9933);
#7065=LINE('',#40637,#9934);
#7066=LINE('',#40640,#9935);
#7067=LINE('',#40641,#9936);
#7068=LINE('',#40647,#9937);
#7069=LINE('',#40648,#9938);
#7070=LINE('',#40651,#9939);
#7071=LINE('',#40652,#9940);
#7072=LINE('',#40654,#9941);
#7073=LINE('',#40657,#9942);
#7074=LINE('',#40676,#9943);
#7075=LINE('',#40680,#9944);
#7076=LINE('',#40685,#9945);
#9870=VECTOR('',#32248,10.);
#9871=VECTOR('',#32249,10.);
#9872=VECTOR('',#32250,10.);
#9873=VECTOR('',#32253,10.);
#9874=VECTOR('',#32254,10.);
#9875=VECTOR('',#32255,10.);
#9876=VECTOR('',#32258,10.);
#9877=VECTOR('',#32259,10.);
#9878=VECTOR('',#32260,10.);
#9879=VECTOR('',#32263,10.);
#9880=VECTOR('',#32264,10.);
#9881=VECTOR('',#32265,10.);
#9882=VECTOR('',#32268,10.);
#9883=VECTOR('',#32269,10.);
#9884=VECTOR('',#32272,10.);
#9885=VECTOR('',#32273,10.);
#9886=VECTOR('',#32274,10.);
#9887=VECTOR('',#32277,10.);
#9888=VECTOR('',#32278,10.);
#9889=VECTOR('',#32279,10.);
#9890=VECTOR('',#32282,10.);
#9891=VECTOR('',#32283,10.);
#9892=VECTOR('',#32286,10.);
#9893=VECTOR('',#32287,10.);
#9894=VECTOR('',#32290,10.);
#9895=VECTOR('',#32291,10.);
#9896=VECTOR('',#32294,10.);
#9897=VECTOR('',#32295,10.);
#9898=VECTOR('',#32298,10.);
#9899=VECTOR('',#32299,10.);
#9900=VECTOR('',#32302,10.);
#9901=VECTOR('',#32303,10.);
#9902=VECTOR('',#32306,10.);
#9903=VECTOR('',#32307,10.);
#9904=VECTOR('',#32310,10.);
#9905=VECTOR('',#32311,10.);
#9906=VECTOR('',#32314,10.);
#9907=VECTOR('',#32315,10.);
#9908=VECTOR('',#32318,10.);
#9909=VECTOR('',#32319,10.);
#9910=VECTOR('',#32322,10.);
#9911=VECTOR('',#32323,10.);
#9912=VECTOR('',#32336,10.);
#9913=VECTOR('',#32337,10.);
#9914=VECTOR('',#32338,10.);
#9915=VECTOR('',#32339,10.);
#9916=VECTOR('',#32342,10.);
#9917=VECTOR('',#32343,10.);
#9918=VECTOR('',#32344,10.);
#9919=VECTOR('',#32347,10.);
#9920=VECTOR('',#32348,10.);
#9921=VECTOR('',#32349,10.);
#9922=VECTOR('',#32350,10.);
#9923=VECTOR('',#32353,10.);
#9924=VECTOR('',#32354,10.);
#9925=VECTOR('',#32355,10.);
#9926=VECTOR('',#32358,10.);
#9927=VECTOR('',#32359,10.);
#9928=VECTOR('',#32362,10.);
#9929=VECTOR('',#32363,10.);
#9930=VECTOR('',#32366,10.);
#9931=VECTOR('',#32367,10.);
#9932=VECTOR('',#32368,10.);
#9933=VECTOR('',#32371,10.);
#9934=VECTOR('',#32372,10.);
#9935=VECTOR('',#32375,10.);
#9936=VECTOR('',#32376,10.);
#9937=VECTOR('',#32383,10.);
#9938=VECTOR('',#32384,10.);
#9939=VECTOR('',#32387,10.);
#9940=VECTOR('',#32388,10.);
#9941=VECTOR('',#32391,10.);
#9942=VECTOR('',#32396,9.4);
#9943=VECTOR('',#32411,6.89);
#9944=VECTOR('',#32416,7.14);
#9945=VECTOR('',#32423,6.2);
#10624=CIRCLE('',#26551,6.2);
#10625=CIRCLE('',#26562,8.4732);
#10626=CIRCLE('',#26572,6.64);
#10627=CIRCLE('',#26574,7.14);
#10628=CIRCLE('',#26576,7.14);
#10629=CIRCLE('',#26578,6.2);
#12619=VERTEX_POINT('',#40466);
#12620=VERTEX_POINT('',#40467);
#12621=VERTEX_POINT('',#40469);
#12622=VERTEX_POINT('',#40473);
#12623=VERTEX_POINT('',#40474);
#12624=VERTEX_POINT('',#40476);
#12625=VERTEX_POINT('',#40480);
#12626=VERTEX_POINT('',#40481);
#12627=VERTEX_POINT('',#40483);
#12628=VERTEX_POINT('',#40487);
#12629=VERTEX_POINT('',#40488);
#12630=VERTEX_POINT('',#40490);
#12631=VERTEX_POINT('',#40497);
#12632=VERTEX_POINT('',#40498);
#12633=VERTEX_POINT('',#40500);
#12634=VERTEX_POINT('',#40504);
#12635=VERTEX_POINT('',#40505);
#12636=VERTEX_POINT('',#40507);
#12637=VERTEX_POINT('',#40517);
#12638=VERTEX_POINT('',#40518);
#12639=VERTEX_POINT('',#40528);
#12640=VERTEX_POINT('',#40529);
#12641=VERTEX_POINT('',#40536);
#12642=VERTEX_POINT('',#40537);
#12643=VERTEX_POINT('',#40547);
#12644=VERTEX_POINT('',#40548);
#12645=VERTEX_POINT('',#40555);
#12646=VERTEX_POINT('',#40556);
#12647=VERTEX_POINT('',#40566);
#12648=VERTEX_POINT('',#40567);
#12649=VERTEX_POINT('',#40578);
#12650=VERTEX_POINT('',#40590);
#12651=VERTEX_POINT('',#40593);
#12652=VERTEX_POINT('',#40594);
#12653=VERTEX_POINT('',#40596);
#12654=VERTEX_POINT('',#40598);
#12655=VERTEX_POINT('',#40602);
#12656=VERTEX_POINT('',#40604);
#12657=VERTEX_POINT('',#40608);
#12658=VERTEX_POINT('',#40609);
#12659=VERTEX_POINT('',#40611);
#12660=VERTEX_POINT('',#40613);
#12661=VERTEX_POINT('',#40617);
#12662=VERTEX_POINT('',#40619);
#12663=VERTEX_POINT('',#40629);
#12664=VERTEX_POINT('',#40631);
#12665=VERTEX_POINT('',#40635);
#12666=VERTEX_POINT('',#40639);
#12667=VERTEX_POINT('',#40643);
#12668=VERTEX_POINT('',#40646);
#12669=VERTEX_POINT('',#40650);
#12670=VERTEX_POINT('',#40671);
#12671=VERTEX_POINT('',#40674);
#12672=VERTEX_POINT('',#40678);
#12673=VERTEX_POINT('',#40682);
#15914=EDGE_CURVE('',#12619,#12620,#7001,.T.);
#15915=EDGE_CURVE('',#12621,#12619,#7002,.T.);
#15916=EDGE_CURVE('',#12620,#12621,#7003,.T.);
#15917=EDGE_CURVE('',#12622,#12623,#7004,.T.);
#15918=EDGE_CURVE('',#12624,#12622,#7005,.T.);
#15919=EDGE_CURVE('',#12623,#12624,#7006,.T.);
#15920=EDGE_CURVE('',#12625,#12626,#7007,.T.);
#15921=EDGE_CURVE('',#12627,#12625,#7008,.T.);
#15922=EDGE_CURVE('',#12626,#12627,#7009,.T.);
#15923=EDGE_CURVE('',#12628,#12629,#7010,.T.);
#15924=EDGE_CURVE('',#12630,#12628,#7011,.T.);
#15925=EDGE_CURVE('',#12629,#12630,#7012,.T.);
#15926=EDGE_CURVE('',#12628,#12624,#7013,.T.);
#15927=EDGE_CURVE('',#12622,#12630,#7014,.T.);
#15928=EDGE_CURVE('',#12631,#12632,#7015,.T.);
#15929=EDGE_CURVE('',#12633,#12631,#7016,.T.);
#15930=EDGE_CURVE('',#12632,#12633,#7017,.T.);
#15931=EDGE_CURVE('',#12634,#12635,#7018,.T.);
#15932=EDGE_CURVE('',#12636,#12634,#7019,.T.);
#15933=EDGE_CURVE('',#12635,#12636,#7020,.T.);
#15934=EDGE_CURVE('',#12634,#12629,#7021,.T.);
#15935=EDGE_CURVE('',#12630,#12636,#7022,.T.);
#15936=EDGE_CURVE('',#12631,#12635,#7023,.T.);
#15937=EDGE_CURVE('',#12636,#12633,#7024,.T.);
#15938=EDGE_CURVE('',#12637,#12638,#123,.T.);
#15939=EDGE_CURVE('',#12638,#12634,#7025,.T.);
#15940=EDGE_CURVE('',#12635,#12637,#7026,.T.);
#15941=EDGE_CURVE('',#12625,#12632,#7027,.T.);
#15942=EDGE_CURVE('',#12633,#12627,#7028,.T.);
#15943=EDGE_CURVE('',#12639,#12640,#124,.T.);
#15944=EDGE_CURVE('',#12640,#12631,#7029,.T.);
#15945=EDGE_CURVE('',#12632,#12639,#7030,.T.);
#15946=EDGE_CURVE('',#12641,#12642,#125,.T.);
#15947=EDGE_CURVE('',#12642,#12628,#7031,.T.);
#15948=EDGE_CURVE('',#12629,#12641,#7032,.T.);
#15949=EDGE_CURVE('',#12619,#12626,#7033,.T.);
#15950=EDGE_CURVE('',#12627,#12621,#7034,.T.);
#15951=EDGE_CURVE('',#12643,#12644,#126,.T.);
#15952=EDGE_CURVE('',#12644,#12625,#7035,.T.);
#15953=EDGE_CURVE('',#12626,#12643,#7036,.T.);
#15954=EDGE_CURVE('',#12645,#12646,#127,.T.);
#15955=EDGE_CURVE('',#12646,#12623,#7037,.T.);
#15956=EDGE_CURVE('',#12624,#12645,#7038,.T.);
#15957=EDGE_CURVE('',#12623,#12620,#7039,.T.);
#15958=EDGE_CURVE('',#12621,#12622,#7040,.T.);
#15959=EDGE_CURVE('',#12647,#12648,#128,.T.);
#15960=EDGE_CURVE('',#12648,#12619,#7041,.T.);
#15961=EDGE_CURVE('',#12620,#12647,#7042,.T.);
#15962=EDGE_CURVE('',#12640,#12637,#129,.T.);
#15963=EDGE_CURVE('',#12644,#12649,#130,.T.);
#15964=EDGE_CURVE('',#12649,#12639,#131,.T.);
#15965=EDGE_CURVE('',#12648,#12643,#132,.T.);
#15966=EDGE_CURVE('',#12650,#12650,#10624,.T.);
#15967=EDGE_CURVE('',#12651,#12652,#7043,.T.);
#15968=EDGE_CURVE('',#12652,#12653,#7044,.T.);
#15969=EDGE_CURVE('',#12653,#12654,#7045,.T.);
#15970=EDGE_CURVE('',#12651,#12654,#7046,.T.);
#15971=EDGE_CURVE('',#12652,#12655,#7047,.T.);
#15972=EDGE_CURVE('',#12655,#12656,#7048,.T.);
#15973=EDGE_CURVE('',#12656,#12653,#7049,.T.);
#15974=EDGE_CURVE('',#12657,#12658,#7050,.T.);
#15975=EDGE_CURVE('',#12658,#12659,#7051,.T.);
#15976=EDGE_CURVE('',#12659,#12660,#7052,.T.);
#15977=EDGE_CURVE('',#12660,#12657,#7053,.T.);
#15978=EDGE_CURVE('',#12661,#12659,#7054,.T.);
#15979=EDGE_CURVE('',#12658,#12662,#7055,.T.);
#15980=EDGE_CURVE('',#12662,#12661,#7056,.T.);
#15981=EDGE_CURVE('',#12655,#12657,#7057,.T.);
#15982=EDGE_CURVE('',#12660,#12656,#7058,.T.);
#15983=EDGE_CURVE('',#12654,#12661,#7059,.T.);
#15984=EDGE_CURVE('',#12662,#12651,#7060,.T.);
#15985=EDGE_CURVE('',#12656,#12663,#7061,.T.);
#15986=EDGE_CURVE('',#12663,#12664,#7062,.T.);
#15987=EDGE_CURVE('',#12653,#12664,#7063,.T.);
#15988=EDGE_CURVE('',#12660,#12665,#7064,.T.);
#15989=EDGE_CURVE('',#12665,#12663,#7065,.T.);
#15990=EDGE_CURVE('',#12659,#12666,#7066,.T.);
#15991=EDGE_CURVE('',#12666,#12665,#7067,.T.);
#15992=EDGE_CURVE('',#12667,#12667,#10625,.T.);
#15993=EDGE_CURVE('',#12661,#12668,#7068,.T.);
#15994=EDGE_CURVE('',#12668,#12666,#7069,.T.);
#15995=EDGE_CURVE('',#12654,#12669,#7070,.T.);
#15996=EDGE_CURVE('',#12669,#12668,#7071,.T.);
#15997=EDGE_CURVE('',#12664,#12669,#7072,.T.);
#15998=EDGE_CURVE('',#12649,#12667,#7073,.T.);
#15999=EDGE_CURVE('',#12646,#12647,#133,.T.);
#16000=EDGE_CURVE('',#12642,#12645,#134,.T.);
#16001=EDGE_CURVE('',#12638,#12641,#135,.T.);
#16002=EDGE_CURVE('',#12670,#12670,#10626,.T.);
#16003=EDGE_CURVE('',#12671,#12671,#10627,.T.);
#16004=EDGE_CURVE('',#12671,#12670,#7074,.T.);
#16005=EDGE_CURVE('',#12672,#12672,#10628,.T.);
#16006=EDGE_CURVE('',#12672,#12671,#7075,.T.);
#16007=EDGE_CURVE('',#12673,#12673,#10629,.T.);
#16008=EDGE_CURVE('',#12650,#12673,#7076,.T.);
#22322=ORIENTED_EDGE('',*,*,#15914,.F.);
#22323=ORIENTED_EDGE('',*,*,#15915,.F.);
#22324=ORIENTED_EDGE('',*,*,#15916,.F.);
#22325=ORIENTED_EDGE('',*,*,#15917,.F.);
#22326=ORIENTED_EDGE('',*,*,#15918,.F.);
#22327=ORIENTED_EDGE('',*,*,#15919,.F.);
#22328=ORIENTED_EDGE('',*,*,#15920,.F.);
#22329=ORIENTED_EDGE('',*,*,#15921,.F.);
#22330=ORIENTED_EDGE('',*,*,#15922,.F.);
#22331=ORIENTED_EDGE('',*,*,#15923,.F.);
#22332=ORIENTED_EDGE('',*,*,#15924,.F.);
#22333=ORIENTED_EDGE('',*,*,#15925,.F.);
#22334=ORIENTED_EDGE('',*,*,#15924,.T.);
#22335=ORIENTED_EDGE('',*,*,#15926,.T.);
#22336=ORIENTED_EDGE('',*,*,#15918,.T.);
#22337=ORIENTED_EDGE('',*,*,#15927,.T.);
#22338=ORIENTED_EDGE('',*,*,#15928,.F.);
#22339=ORIENTED_EDGE('',*,*,#15929,.F.);
#22340=ORIENTED_EDGE('',*,*,#15930,.F.);
#22341=ORIENTED_EDGE('',*,*,#15931,.F.);
#22342=ORIENTED_EDGE('',*,*,#15932,.F.);
#22343=ORIENTED_EDGE('',*,*,#15933,.F.);
#22344=ORIENTED_EDGE('',*,*,#15932,.T.);
#22345=ORIENTED_EDGE('',*,*,#15934,.T.);
#22346=ORIENTED_EDGE('',*,*,#15925,.T.);
#22347=ORIENTED_EDGE('',*,*,#15935,.T.);
#22348=ORIENTED_EDGE('',*,*,#15929,.T.);
#22349=ORIENTED_EDGE('',*,*,#15936,.T.);
#22350=ORIENTED_EDGE('',*,*,#15933,.T.);
#22351=ORIENTED_EDGE('',*,*,#15937,.T.);
#22352=ORIENTED_EDGE('',*,*,#15938,.T.);
#22353=ORIENTED_EDGE('',*,*,#15939,.T.);
#22354=ORIENTED_EDGE('',*,*,#15931,.T.);
#22355=ORIENTED_EDGE('',*,*,#15940,.T.);
#22356=ORIENTED_EDGE('',*,*,#15921,.T.);
#22357=ORIENTED_EDGE('',*,*,#15941,.T.);
#22358=ORIENTED_EDGE('',*,*,#15930,.T.);
#22359=ORIENTED_EDGE('',*,*,#15942,.T.);
#22360=ORIENTED_EDGE('',*,*,#15943,.T.);
#22361=ORIENTED_EDGE('',*,*,#15944,.T.);
#22362=ORIENTED_EDGE('',*,*,#15928,.T.);
#22363=ORIENTED_EDGE('',*,*,#15945,.T.);
#22364=ORIENTED_EDGE('',*,*,#15946,.T.);
#22365=ORIENTED_EDGE('',*,*,#15947,.T.);
#22366=ORIENTED_EDGE('',*,*,#15923,.T.);
#22367=ORIENTED_EDGE('',*,*,#15948,.T.);
#22368=ORIENTED_EDGE('',*,*,#15915,.T.);
#22369=ORIENTED_EDGE('',*,*,#15949,.T.);
#22370=ORIENTED_EDGE('',*,*,#15922,.T.);
#22371=ORIENTED_EDGE('',*,*,#15950,.T.);
#22372=ORIENTED_EDGE('',*,*,#15951,.T.);
#22373=ORIENTED_EDGE('',*,*,#15952,.T.);
#22374=ORIENTED_EDGE('',*,*,#15920,.T.);
#22375=ORIENTED_EDGE('',*,*,#15953,.T.);
#22376=ORIENTED_EDGE('',*,*,#15954,.T.);
#22377=ORIENTED_EDGE('',*,*,#15955,.T.);
#22378=ORIENTED_EDGE('',*,*,#15919,.T.);
#22379=ORIENTED_EDGE('',*,*,#15956,.T.);
#22380=ORIENTED_EDGE('',*,*,#15917,.T.);
#22381=ORIENTED_EDGE('',*,*,#15957,.T.);
#22382=ORIENTED_EDGE('',*,*,#15916,.T.);
#22383=ORIENTED_EDGE('',*,*,#15958,.T.);
#22384=ORIENTED_EDGE('',*,*,#15959,.T.);
#22385=ORIENTED_EDGE('',*,*,#15960,.T.);
#22386=ORIENTED_EDGE('',*,*,#15914,.T.);
#22387=ORIENTED_EDGE('',*,*,#15961,.T.);
#22388=ORIENTED_EDGE('',*,*,#15940,.F.);
#22389=ORIENTED_EDGE('',*,*,#15936,.F.);
#22390=ORIENTED_EDGE('',*,*,#15944,.F.);
#22391=ORIENTED_EDGE('',*,*,#15962,.T.);
#22392=ORIENTED_EDGE('',*,*,#15945,.F.);
#22393=ORIENTED_EDGE('',*,*,#15941,.F.);
#22394=ORIENTED_EDGE('',*,*,#15952,.F.);
#22395=ORIENTED_EDGE('',*,*,#15963,.T.);
#22396=ORIENTED_EDGE('',*,*,#15964,.T.);
#22397=ORIENTED_EDGE('',*,*,#15953,.F.);
#22398=ORIENTED_EDGE('',*,*,#15949,.F.);
#22399=ORIENTED_EDGE('',*,*,#15960,.F.);
#22400=ORIENTED_EDGE('',*,*,#15965,.T.);
#22401=ORIENTED_EDGE('',*,*,#15927,.F.);
#22402=ORIENTED_EDGE('',*,*,#15958,.F.);
#22403=ORIENTED_EDGE('',*,*,#15950,.F.);
#22404=ORIENTED_EDGE('',*,*,#15942,.F.);
#22405=ORIENTED_EDGE('',*,*,#15937,.F.);
#22406=ORIENTED_EDGE('',*,*,#15935,.F.);
#22407=ORIENTED_EDGE('',*,*,#15966,.T.);
#22408=ORIENTED_EDGE('',*,*,#15967,.T.);
#22409=ORIENTED_EDGE('',*,*,#15968,.T.);
#22410=ORIENTED_EDGE('',*,*,#15969,.T.);
#22411=ORIENTED_EDGE('',*,*,#15970,.F.);
#22412=ORIENTED_EDGE('',*,*,#15971,.T.);
#22413=ORIENTED_EDGE('',*,*,#15972,.T.);
#22414=ORIENTED_EDGE('',*,*,#15973,.T.);
#22415=ORIENTED_EDGE('',*,*,#15968,.F.);
#22416=ORIENTED_EDGE('',*,*,#15974,.T.);
#22417=ORIENTED_EDGE('',*,*,#15975,.T.);
#22418=ORIENTED_EDGE('',*,*,#15976,.T.);
#22419=ORIENTED_EDGE('',*,*,#15977,.T.);
#22420=ORIENTED_EDGE('',*,*,#15978,.T.);
#22421=ORIENTED_EDGE('',*,*,#15975,.F.);
#22422=ORIENTED_EDGE('',*,*,#15979,.T.);
#22423=ORIENTED_EDGE('',*,*,#15980,.T.);
#22424=ORIENTED_EDGE('',*,*,#15981,.T.);
#22425=ORIENTED_EDGE('',*,*,#15977,.F.);
#22426=ORIENTED_EDGE('',*,*,#15982,.T.);
#22427=ORIENTED_EDGE('',*,*,#15972,.F.);
#22428=ORIENTED_EDGE('',*,*,#15983,.T.);
#22429=ORIENTED_EDGE('',*,*,#15980,.F.);
#22430=ORIENTED_EDGE('',*,*,#15984,.T.);
#22431=ORIENTED_EDGE('',*,*,#15970,.T.);
#22432=ORIENTED_EDGE('',*,*,#15973,.F.);
#22433=ORIENTED_EDGE('',*,*,#15985,.T.);
#22434=ORIENTED_EDGE('',*,*,#15986,.T.);
#22435=ORIENTED_EDGE('',*,*,#15987,.F.);
#22436=ORIENTED_EDGE('',*,*,#15982,.F.);
#22437=ORIENTED_EDGE('',*,*,#15988,.T.);
#22438=ORIENTED_EDGE('',*,*,#15989,.T.);
#22439=ORIENTED_EDGE('',*,*,#15985,.F.);
#22440=ORIENTED_EDGE('',*,*,#15976,.F.);
#22441=ORIENTED_EDGE('',*,*,#15990,.T.);
#22442=ORIENTED_EDGE('',*,*,#15991,.T.);
#22443=ORIENTED_EDGE('',*,*,#15988,.F.);
#22444=ORIENTED_EDGE('',*,*,#15992,.T.);
#22445=ORIENTED_EDGE('',*,*,#15974,.F.);
#22446=ORIENTED_EDGE('',*,*,#15981,.F.);
#22447=ORIENTED_EDGE('',*,*,#15971,.F.);
#22448=ORIENTED_EDGE('',*,*,#15967,.F.);
#22449=ORIENTED_EDGE('',*,*,#15984,.F.);
#22450=ORIENTED_EDGE('',*,*,#15979,.F.);
#22451=ORIENTED_EDGE('',*,*,#15978,.F.);
#22452=ORIENTED_EDGE('',*,*,#15993,.T.);
#22453=ORIENTED_EDGE('',*,*,#15994,.T.);
#22454=ORIENTED_EDGE('',*,*,#15990,.F.);
#22455=ORIENTED_EDGE('',*,*,#15983,.F.);
#22456=ORIENTED_EDGE('',*,*,#15995,.T.);
#22457=ORIENTED_EDGE('',*,*,#15996,.T.);
#22458=ORIENTED_EDGE('',*,*,#15993,.F.);
#22459=ORIENTED_EDGE('',*,*,#15969,.F.);
#22460=ORIENTED_EDGE('',*,*,#15987,.T.);
#22461=ORIENTED_EDGE('',*,*,#15997,.T.);
#22462=ORIENTED_EDGE('',*,*,#15995,.F.);
#22463=ORIENTED_EDGE('',*,*,#15989,.F.);
#22464=ORIENTED_EDGE('',*,*,#15991,.F.);
#22465=ORIENTED_EDGE('',*,*,#15994,.F.);
#22466=ORIENTED_EDGE('',*,*,#15996,.F.);
#22467=ORIENTED_EDGE('',*,*,#15997,.F.);
#22468=ORIENTED_EDGE('',*,*,#15986,.F.);
#22469=ORIENTED_EDGE('',*,*,#15938,.F.);
#22470=ORIENTED_EDGE('',*,*,#15962,.F.);
#22471=ORIENTED_EDGE('',*,*,#15943,.F.);
#22472=ORIENTED_EDGE('',*,*,#15964,.F.);
#22473=ORIENTED_EDGE('',*,*,#15998,.T.);
#22474=ORIENTED_EDGE('',*,*,#15992,.F.);
#22475=ORIENTED_EDGE('',*,*,#15998,.F.);
#22476=ORIENTED_EDGE('',*,*,#15963,.F.);
#22477=ORIENTED_EDGE('',*,*,#15951,.F.);
#22478=ORIENTED_EDGE('',*,*,#15965,.F.);
#22479=ORIENTED_EDGE('',*,*,#15959,.F.);
#22480=ORIENTED_EDGE('',*,*,#15999,.F.);
#22481=ORIENTED_EDGE('',*,*,#15954,.F.);
#22482=ORIENTED_EDGE('',*,*,#16000,.F.);
#22483=ORIENTED_EDGE('',*,*,#15946,.F.);
#22484=ORIENTED_EDGE('',*,*,#16001,.F.);
#22485=ORIENTED_EDGE('',*,*,#15939,.F.);
#22486=ORIENTED_EDGE('',*,*,#16001,.T.);
#22487=ORIENTED_EDGE('',*,*,#15948,.F.);
#22488=ORIENTED_EDGE('',*,*,#15934,.F.);
#22489=ORIENTED_EDGE('',*,*,#15947,.F.);
#22490=ORIENTED_EDGE('',*,*,#16000,.T.);
#22491=ORIENTED_EDGE('',*,*,#15956,.F.);
#22492=ORIENTED_EDGE('',*,*,#15926,.F.);
#22493=ORIENTED_EDGE('',*,*,#15955,.F.);
#22494=ORIENTED_EDGE('',*,*,#15999,.T.);
#22495=ORIENTED_EDGE('',*,*,#15961,.F.);
#22496=ORIENTED_EDGE('',*,*,#15957,.F.);
#22497=ORIENTED_EDGE('',*,*,#16002,.F.);
#22498=ORIENTED_EDGE('',*,*,#16003,.F.);
#22499=ORIENTED_EDGE('',*,*,#16004,.T.);
#22500=ORIENTED_EDGE('',*,*,#16002,.T.);
#22501=ORIENTED_EDGE('',*,*,#16004,.F.);
#22502=ORIENTED_EDGE('',*,*,#16005,.F.);
#22503=ORIENTED_EDGE('',*,*,#16006,.T.);
#22504=ORIENTED_EDGE('',*,*,#16003,.T.);
#22505=ORIENTED_EDGE('',*,*,#16006,.F.);
#22506=ORIENTED_EDGE('',*,*,#16005,.T.);
#22507=ORIENTED_EDGE('',*,*,#16007,.F.);
#22508=ORIENTED_EDGE('',*,*,#15966,.F.);
#22509=ORIENTED_EDGE('',*,*,#16008,.T.);
#22510=ORIENTED_EDGE('',*,*,#16007,.T.);
#22511=ORIENTED_EDGE('',*,*,#16008,.F.);
#23599=CONICAL_SURFACE('',#26567,9.4,1.04718484902493);
#23600=CONICAL_SURFACE('',#26573,6.89,0.785398163397448);
#24669=ADVANCED_FACE('',(#2810),#1542,.T.);
#24670=ADVANCED_FACE('',(#2811),#1543,.T.);
#24671=ADVANCED_FACE('',(#2812),#1544,.T.);
#24672=ADVANCED_FACE('',(#2813),#1545,.T.);
#24673=ADVANCED_FACE('',(#2814),#1546,.T.);
#24674=ADVANCED_FACE('',(#2815),#1547,.T.);
#24675=ADVANCED_FACE('',(#2816),#1548,.T.);
#24676=ADVANCED_FACE('',(#2817),#1549,.T.);
#24677=ADVANCED_FACE('',(#2818),#1550,.T.);
#24678=ADVANCED_FACE('',(#2819),#1551,.T.);
#24679=ADVANCED_FACE('',(#2820),#1552,.T.);
#24680=ADVANCED_FACE('',(#2821),#1553,.T.);
#24681=ADVANCED_FACE('',(#2822),#1554,.T.);
#24682=ADVANCED_FACE('',(#2823),#1555,.T.);
#24683=ADVANCED_FACE('',(#2824),#1556,.T.);
#24684=ADVANCED_FACE('',(#2825),#1557,.T.);
#24685=ADVANCED_FACE('',(#2826),#1558,.T.);
#24686=ADVANCED_FACE('',(#2827),#1559,.T.);
#24687=ADVANCED_FACE('',(#2828),#1560,.T.);
#24688=ADVANCED_FACE('',(#2829),#1561,.T.);
#24689=ADVANCED_FACE('',(#2830),#1562,.T.);
#24690=ADVANCED_FACE('',(#2831,#665),#1563,.F.);
#24691=ADVANCED_FACE('',(#2832),#1564,.T.);
#24692=ADVANCED_FACE('',(#2833),#1565,.T.);
#24693=ADVANCED_FACE('',(#2834),#1566,.T.);
#24694=ADVANCED_FACE('',(#2835),#1567,.T.);
#24695=ADVANCED_FACE('',(#2836),#1568,.T.);
#24696=ADVANCED_FACE('',(#2837),#1569,.T.);
#24697=ADVANCED_FACE('',(#2838),#1570,.F.);
#24698=ADVANCED_FACE('',(#2839),#1571,.F.);
#24699=ADVANCED_FACE('',(#2840),#1572,.F.);
#24700=ADVANCED_FACE('',(#2841,#666),#1573,.T.);
#24701=ADVANCED_FACE('',(#2842),#1574,.F.);
#24702=ADVANCED_FACE('',(#2843),#1575,.F.);
#24703=ADVANCED_FACE('',(#2844),#1576,.F.);
#24704=ADVANCED_FACE('',(#2845),#1577,.F.);
#24705=ADVANCED_FACE('',(#2846),#23599,.T.);
#24706=ADVANCED_FACE('',(#2847),#1578,.T.);
#24707=ADVANCED_FACE('',(#2848),#1579,.T.);
#24708=ADVANCED_FACE('',(#2849),#1580,.T.);
#24709=ADVANCED_FACE('',(#2850),#1581,.T.);
#24710=ADVANCED_FACE('',(#2851),#23600,.T.);
#24711=ADVANCED_FACE('',(#2852),#532,.T.);
#24712=ADVANCED_FACE('',(#2853,#667),#1582,.T.);
#24713=ADVANCED_FACE('',(#2854),#533,.T.);
#24947=CLOSED_SHELL('',(#24669,#24670,#24671,#24672,#24673,#24674,#24675,
#24676,#24677,#24678,#24679,#24680,#24681,#24682,#24683,#24684,#24685,#24686,
#24687,#24688,#24689,#24690,#24691,#24692,#24693,#24694,#24695,#24696,#24697,
#24698,#24699,#24700,#24701,#24702,#24703,#24704,#24705,#24706,#24707,#24708,
#24709,#24710,#24711,#24712,#24713));
#26528=AXIS2_PLACEMENT_3D('',#40464,#32244,#32245);
#26529=AXIS2_PLACEMENT_3D('',#40465,#32246,#32247);
#26530=AXIS2_PLACEMENT_3D('',#40472,#32251,#32252);
#26531=AXIS2_PLACEMENT_3D('',#40479,#32256,#32257);
#26532=AXIS2_PLACEMENT_3D('',#40486,#32261,#32262);
#26533=AXIS2_PLACEMENT_3D('',#40493,#32266,#32267);
#26534=AXIS2_PLACEMENT_3D('',#40496,#32270,#32271);
#26535=AXIS2_PLACEMENT_3D('',#40503,#32275,#32276);
#26536=AXIS2_PLACEMENT_3D('',#40510,#32280,#32281);
#26537=AXIS2_PLACEMENT_3D('',#40513,#32284,#32285);
#26538=AXIS2_PLACEMENT_3D('',#40516,#32288,#32289);
#26539=AXIS2_PLACEMENT_3D('',#40524,#32292,#32293);
#26540=AXIS2_PLACEMENT_3D('',#40527,#32296,#32297);
#26541=AXIS2_PLACEMENT_3D('',#40535,#32300,#32301);
#26542=AXIS2_PLACEMENT_3D('',#40543,#32304,#32305);
#26543=AXIS2_PLACEMENT_3D('',#40546,#32308,#32309);
#26544=AXIS2_PLACEMENT_3D('',#40554,#32312,#32313);
#26545=AXIS2_PLACEMENT_3D('',#40562,#32316,#32317);
#26546=AXIS2_PLACEMENT_3D('',#40565,#32320,#32321);
#26547=AXIS2_PLACEMENT_3D('',#40573,#32324,#32325);
#26548=AXIS2_PLACEMENT_3D('',#40577,#32326,#32327);
#26549=AXIS2_PLACEMENT_3D('',#40585,#32328,#32329);
#26550=AXIS2_PLACEMENT_3D('',#40589,#32330,#32331);
#26551=AXIS2_PLACEMENT_3D('',#40591,#32332,#32333);
#26552=AXIS2_PLACEMENT_3D('',#40592,#32334,#32335);
#26553=AXIS2_PLACEMENT_3D('',#40601,#32340,#32341);
#26554=AXIS2_PLACEMENT_3D('',#40607,#32345,#32346);
#26555=AXIS2_PLACEMENT_3D('',#40616,#32351,#32352);
#26556=AXIS2_PLACEMENT_3D('',#40622,#32356,#32357);
#26557=AXIS2_PLACEMENT_3D('',#40625,#32360,#32361);
#26558=AXIS2_PLACEMENT_3D('',#40628,#32364,#32365);
#26559=AXIS2_PLACEMENT_3D('',#40634,#32369,#32370);
#26560=AXIS2_PLACEMENT_3D('',#40638,#32373,#32374);
#26561=AXIS2_PLACEMENT_3D('',#40642,#32377,#32378);
#26562=AXIS2_PLACEMENT_3D('',#40644,#32379,#32380);
#26563=AXIS2_PLACEMENT_3D('',#40645,#32381,#32382);
#26564=AXIS2_PLACEMENT_3D('',#40649,#32385,#32386);
#26565=AXIS2_PLACEMENT_3D('',#40653,#32389,#32390);
#26566=AXIS2_PLACEMENT_3D('',#40655,#32392,#32393);
#26567=AXIS2_PLACEMENT_3D('',#40656,#32394,#32395);
#26568=AXIS2_PLACEMENT_3D('',#40667,#32397,#32398);
#26569=AXIS2_PLACEMENT_3D('',#40668,#32399,#32400);
#26570=AXIS2_PLACEMENT_3D('',#40669,#32401,#32402);
#26571=AXIS2_PLACEMENT_3D('',#40670,#32403,#32404);
#26572=AXIS2_PLACEMENT_3D('',#40672,#32405,#32406);
#26573=AXIS2_PLACEMENT_3D('',#40673,#32407,#32408);
#26574=AXIS2_PLACEMENT_3D('',#40675,#32409,#32410);
#26575=AXIS2_PLACEMENT_3D('',#40677,#32412,#32413);
#26576=AXIS2_PLACEMENT_3D('',#40679,#32414,#32415);
#26577=AXIS2_PLACEMENT_3D('',#40681,#32417,#32418);
#26578=AXIS2_PLACEMENT_3D('',#40683,#32419,#32420);
#26579=AXIS2_PLACEMENT_3D('',#40684,#32421,#32422);
#32244=DIRECTION('axis',(0.,0.,1.));
#32245=DIRECTION('refdir',(1.,0.,0.));
#32246=DIRECTION('center_axis',(-0.54775000523585,5.84175495892749E-17,
-0.836642057133232));
#32247=DIRECTION('ref_axis',(-0.836642057133232,0.,0.54775000523585));
#32248=DIRECTION('',(0.,1.,1.28197512425571E-15));
#32249=DIRECTION('',(0.677497944020808,-0.586730430533752,-0.443558268701257));
#32250=DIRECTION('',(-0.677497944020811,-0.586730430533747,0.443558268701259));
#32251=DIRECTION('center_axis',(-0.54775000523585,0.724553275351851,-0.418321028566616));
#32252=DIRECTION('ref_axis',(-0.606949534647158,0.,0.79474037420506));
#32253=DIRECTION('',(0.677497944020812,0.0907675134870681,-0.729902592366233));
#32254=DIRECTION('',(-0.677497944020808,-0.677497944020809,-0.286344323664981));
#32255=DIRECTION('',(0.,0.499999999999999,0.866025403784439));
#32256=DIRECTION('center_axis',(-0.547750005235851,-0.72455327535185,-0.418321028566615));
#32257=DIRECTION('ref_axis',(-0.606949534647157,0.,0.79474037420506));
#32258=DIRECTION('',(0.,0.499999999999999,-0.866025403784439));
#32259=DIRECTION('',(0.677497944020809,-0.677497944020809,0.286344323664978));
#32260=DIRECTION('',(-0.677497944020809,0.0907675134870617,0.729902592366237));
#32261=DIRECTION('center_axis',(-0.54775000523585,0.724553275351851,0.418321028566614));
#32262=DIRECTION('ref_axis',(0.606949534647157,0.,0.794740374205061));
#32263=DIRECTION('',(0.,-0.5,0.866025403784439));
#32264=DIRECTION('',(0.677497944020808,0.677497944020808,-0.286344323664982));
#32265=DIRECTION('',(-0.677497944020809,-0.0907675134870617,-0.729902592366237));
#32266=DIRECTION('center_axis',(-0.707106781186548,0.707106781186547,-2.33098278087517E-16));
#32267=DIRECTION('ref_axis',(-3.29650746237182E-16,0.,1.));
#32268=DIRECTION('',(0.,-3.29650746237182E-16,-1.));
#32269=DIRECTION('',(0.,3.29650746237182E-16,1.));
#32270=DIRECTION('center_axis',(-0.547750005235851,-0.724553275351851,0.418321028566615));
#32271=DIRECTION('ref_axis',(0.606949534647157,0.,0.79474037420506));
#32272=DIRECTION('',(0.,-0.5,-0.866025403784439));
#32273=DIRECTION('',(0.677497944020811,-0.0907675134870634,0.729902592366235));
#32274=DIRECTION('',(-0.677497944020808,0.677497944020809,0.286344323664979));
#32275=DIRECTION('center_axis',(-0.54775000523585,-1.10993344219622E-15,
0.836642057133232));
#32276=DIRECTION('ref_axis',(0.836642057133232,0.,0.54775000523585));
#32277=DIRECTION('',(0.,-1.,-2.56395024851142E-15));
#32278=DIRECTION('',(0.677497944020809,0.586730430533748,0.44355826870126));
#32279=DIRECTION('',(-0.67749794402081,0.586730430533748,-0.443558268701259));
#32280=DIRECTION('center_axis',(-0.707106781186548,0.353553390593274,0.612372435695794));
#32281=DIRECTION('ref_axis',(0.654653670707977,0.,0.755928946018455));
#32282=DIRECTION('',(0.,0.866025403784439,-0.5));
#32283=DIRECTION('',(0.,-0.866025403784439,0.5));
#32284=DIRECTION('center_axis',(-0.707106781186547,-0.353553390593274,0.612372435695795));
#32285=DIRECTION('ref_axis',(0.654653670707978,0.,0.755928946018454));
#32286=DIRECTION('',(0.,0.866025403784439,0.5));
#32287=DIRECTION('',(0.,-0.866025403784439,-0.5));
#32288=DIRECTION('center_axis',(0.,-2.56395024851142E-15,1.));
#32289=DIRECTION('ref_axis',(1.,0.,0.));
#32290=DIRECTION('',(-1.,0.,0.));
#32291=DIRECTION('',(1.,0.,0.));
#32292=DIRECTION('center_axis',(-0.707106781186548,-0.707106781186547,0.));
#32293=DIRECTION('ref_axis',(0.,0.,1.));
#32294=DIRECTION('',(0.,0.,1.));
#32295=DIRECTION('',(0.,0.,-1.));
#32296=DIRECTION('center_axis',(0.,-0.866025403784439,0.5));
#32297=DIRECTION('ref_axis',(0.,-0.5,-0.866025403784439));
#32298=DIRECTION('',(-1.,0.,0.));
#32299=DIRECTION('',(1.,0.,0.));
#32300=DIRECTION('center_axis',(0.,0.866025403784439,0.5));
#32301=DIRECTION('ref_axis',(0.,-0.5,0.866025403784439));
#32302=DIRECTION('',(-1.,0.,0.));
#32303=DIRECTION('',(1.,0.,0.));
#32304=DIRECTION('center_axis',(-0.707106781186547,-0.353553390593274,-0.612372435695794));
#32305=DIRECTION('ref_axis',(-0.654653670707977,0.,0.755928946018454));
#32306=DIRECTION('',(0.,-0.866025403784439,0.5));
#32307=DIRECTION('',(0.,0.866025403784439,-0.5));
#32308=DIRECTION('center_axis',(0.,-0.866025403784439,-0.5));
#32309=DIRECTION('ref_axis',(0.,0.5,-0.866025403784439));
#32310=DIRECTION('',(-1.,0.,0.));
#32311=DIRECTION('',(1.,0.,0.));
#32312=DIRECTION('center_axis',(0.,0.866025403784439,-0.499999999999999));
#32313=DIRECTION('ref_axis',(0.,0.499999999999999,0.866025403784439));
#32314=DIRECTION('',(-1.,0.,0.));
#32315=DIRECTION('',(1.,0.,0.));
#32316=DIRECTION('center_axis',(-0.707106781186546,0.353553390593275,-0.612372435695796));
#32317=DIRECTION('ref_axis',(-0.654653670707979,0.,0.755928946018453));
#32318=DIRECTION('',(0.,-0.866025403784439,-0.5));
#32319=DIRECTION('',(0.,0.866025403784439,0.5));
#32320=DIRECTION('center_axis',(0.,1.28197512425571E-15,-1.));
#32321=DIRECTION('ref_axis',(-1.,0.,0.));
#32322=DIRECTION('',(-1.,0.,0.));
#32323=DIRECTION('',(1.,0.,0.));
#32324=DIRECTION('center_axis',(0.,-0.5,0.866025403784439));
#32325=DIRECTION('ref_axis',(0.,-0.866025403784439,-0.5));
#32326=DIRECTION('center_axis',(0.,-1.,0.));
#32327=DIRECTION('ref_axis',(0.,0.,-1.));
#32328=DIRECTION('center_axis',(0.,-0.5,-0.866025403784439));
#32329=DIRECTION('ref_axis',(0.,0.866025403784439,-0.5));
#32330=DIRECTION('center_axis',(1.,0.,0.));
#32331=DIRECTION('ref_axis',(0.,0.,-1.));
#32332=DIRECTION('center_axis',(1.,0.,0.));
#32333=DIRECTION('ref_axis',(0.,0.,-1.));
#32334=DIRECTION('center_axis',(0.707106781186547,0.353553390593274,0.612372435695795));
#32335=DIRECTION('ref_axis',(0.654653670707978,0.,-0.755928946018454));
#32336=DIRECTION('',(0.,0.866025403784439,-0.5));
#32337=DIRECTION('',(-0.654653670707977,-4.69765578524213E-16,0.755928946018454));
#32338=DIRECTION('',(0.,-0.866025403784439,0.5));
#32339=DIRECTION('',(-0.654653670707978,0.654653670707977,0.377964473009227));
#32340=DIRECTION('center_axis',(0.707106781186548,-0.353553390593273,0.612372435695795));
#32341=DIRECTION('ref_axis',(0.654653670707977,0.,-0.755928946018455));
#32342=DIRECTION('',(0.,0.866025403784439,0.5));
#32343=DIRECTION('',(-0.654653670707977,-0.654653670707976,0.377964473009229));
#32344=DIRECTION('',(0.,-0.866025403784439,-0.5));
#32345=DIRECTION('center_axis',(0.707106781186547,-0.353553390593274,-0.612372435695795));
#32346=DIRECTION('ref_axis',(-0.654653670707978,0.,-0.755928946018454));
#32347=DIRECTION('',(0.,-0.866025403784439,0.5));
#32348=DIRECTION('',(-0.654653670707977,1.00453536761267E-15,-0.755928946018454));
#32349=DIRECTION('',(0.,0.866025403784439,-0.5));
#32350=DIRECTION('',(0.654653670707978,0.654653670707977,0.377964473009227));
#32351=DIRECTION('center_axis',(0.707106781186548,0.353553390593274,-0.612372435695794));
#32352=DIRECTION('ref_axis',(-0.654653670707977,0.,-0.755928946018455));
#32353=DIRECTION('',(0.,0.866025403784439,0.5));
#32354=DIRECTION('',(0.,-0.866025403784439,-0.5));
#32355=DIRECTION('',(-0.654653670707977,0.654653670707977,-0.377964473009228));
#32356=DIRECTION('center_axis',(0.707106781186547,-0.707106781186548,2.2662332591842E-16));
#32357=DIRECTION('ref_axis',(3.20493781063928E-16,0.,-1.));
#32358=DIRECTION('',(0.,3.20493781063927E-16,1.));
#32359=DIRECTION('',(0.,-3.20493781063927E-16,-1.));
#32360=DIRECTION('center_axis',(0.707106781186547,0.707106781186548,1.1331166295921E-16));
#32361=DIRECTION('ref_axis',(1.60246890531964E-16,0.,-1.));
#32362=DIRECTION('',(0.,-1.60246890531964E-16,1.));
#32363=DIRECTION('',(0.,1.60246890531964E-16,-1.));
#32364=DIRECTION('center_axis',(0.,0.5,-0.866025403784439));
#32365=DIRECTION('ref_axis',(0.,-0.866025403784439,-0.5));
#32366=DIRECTION('',(-1.,0.,0.));
#32367=DIRECTION('',(0.,-0.866025403784439,-0.5));
#32368=DIRECTION('',(-1.,0.,0.));
#32369=DIRECTION('center_axis',(0.,1.,-3.20493781063927E-16));
#32370=DIRECTION('ref_axis',(0.,-3.20493781063927E-16,-1.));
#32371=DIRECTION('',(-1.,0.,0.));
#32372=DIRECTION('',(0.,-3.20493781063927E-16,-1.));
#32373=DIRECTION('center_axis',(0.,0.5,0.866025403784439));
#32374=DIRECTION('ref_axis',(0.,0.866025403784439,-0.5));
#32375=DIRECTION('',(-1.,0.,0.));
#32376=DIRECTION('',(0.,0.866025403784439,-0.5));
#32377=DIRECTION('center_axis',(1.,0.,0.));
#32378=DIRECTION('ref_axis',(0.,0.,-1.));
#32379=DIRECTION('center_axis',(1.,0.,0.));
#32380=DIRECTION('ref_axis',(0.,1.,0.));
#32381=DIRECTION('center_axis',(0.,-0.5,0.866025403784439));
#32382=DIRECTION('ref_axis',(0.,0.866025403784439,0.5));
#32383=DIRECTION('',(-1.,0.,0.));
#32384=DIRECTION('',(0.,0.866025403784439,0.5));
#32385=DIRECTION('center_axis',(0.,-1.,-1.60246890531964E-16));
#32386=DIRECTION('ref_axis',(0.,-1.60246890531964E-16,1.));
#32387=DIRECTION('',(-1.,0.,0.));
#32388=DIRECTION('',(0.,-1.60246890531964E-16,1.));
#32389=DIRECTION('center_axis',(0.,-0.5,-0.866025403784439));
#32390=DIRECTION('ref_axis',(0.,-0.866025403784439,0.5));
#32391=DIRECTION('',(0.,-0.866025403784439,0.5));
#32392=DIRECTION('center_axis',(-1.,0.,0.));
#32393=DIRECTION('ref_axis',(0.,0.,1.));
#32394=DIRECTION('center_axis',(-1.,0.,0.));
#32395=DIRECTION('ref_axis',(0.,1.,0.));
#32396=DIRECTION('',(0.500011000363013,0.866019052628739,1.06056746080241E-16));
#32397=DIRECTION('center_axis',(0.,0.5,0.866025403784439));
#32398=DIRECTION('ref_axis',(0.,-0.866025403784439,0.5));
#32399=DIRECTION('center_axis',(0.,1.,-3.29650746237182E-16));
#32400=DIRECTION('ref_axis',(0.,3.29650746237182E-16,1.));
#32401=DIRECTION('center_axis',(0.,0.5,-0.866025403784439));
#32402=DIRECTION('ref_axis',(0.,0.866025403784439,0.5));
#32403=DIRECTION('center_axis',(-1.,0.,0.));
#32404=DIRECTION('ref_axis',(0.,0.,1.));
#32405=DIRECTION('center_axis',(1.,0.,0.));
#32406=DIRECTION('ref_axis',(0.,0.,-1.));
#32407=DIRECTION('center_axis',(1.,0.,0.));
#32408=DIRECTION('ref_axis',(0.,1.,0.));
#32409=DIRECTION('center_axis',(1.,0.,0.));
#32410=DIRECTION('ref_axis',(0.,0.,-1.));
#32411=DIRECTION('',(-0.707106781186547,0.707106781186548,8.65956056235493E-17));
#32412=DIRECTION('center_axis',(1.,0.,0.));
#32413=DIRECTION('ref_axis',(0.,1.,0.));
#32414=DIRECTION('center_axis',(1.,0.,0.));
#32415=DIRECTION('ref_axis',(0.,0.,-1.));
#32416=DIRECTION('',(-1.,0.,0.));
#32417=DIRECTION('center_axis',(1.,0.,0.));
#32418=DIRECTION('ref_axis',(0.,0.,-1.));
#32419=DIRECTION('center_axis',(1.,0.,0.));
#32420=DIRECTION('ref_axis',(0.,0.,-1.));
#32421=DIRECTION('center_axis',(1.,0.,0.));
#32422=DIRECTION('ref_axis',(0.,1.,0.));
#32423=DIRECTION('',(-1.,0.,0.));
#40464=CARTESIAN_POINT('',(0.,0.,0.));
#40465=CARTESIAN_POINT('Origin',(0.,1.11022302462516E-15,-9.52627944162883));
#40466=CARTESIAN_POINT('',(0.5,-0.433012701892221,-9.85362971081845));
#40467=CARTESIAN_POINT('',(0.5,0.433012701892217,-9.85362971081845));
#40468=CARTESIAN_POINT('',(0.5,-0.433012701892222,-9.85362971081845));
#40469=CARTESIAN_POINT('',(0.,0.,-9.52627944162883));
#40470=CARTESIAN_POINT('',(0.,1.11022302462516E-15,-9.52627944162883));
#40471=CARTESIAN_POINT('',(0.5,0.433012701892217,-9.85362971081845));
#40472=CARTESIAN_POINT('Origin',(0.5,8.75,-4.55181485540923));
#40473=CARTESIAN_POINT('',(0.,8.25,-4.76313972081442));
#40474=CARTESIAN_POINT('',(0.5,8.31698729810778,-5.30181485540923));
#40475=CARTESIAN_POINT('',(0.,8.24999999999999,-4.76313972081442));
#40476=CARTESIAN_POINT('',(0.5,8.75,-4.55181485540923));
#40477=CARTESIAN_POINT('',(0.5,8.75,-4.55181485540923));
#40478=CARTESIAN_POINT('',(0.5,8.31698729810778,-5.30181485540923));
#40479=CARTESIAN_POINT('Origin',(0.,-8.25,-4.76313972081441));
#40480=CARTESIAN_POINT('',(0.5,-8.75,-4.55181485540923));
#40481=CARTESIAN_POINT('',(0.5,-8.31698729810778,-5.30181485540923));
#40482=CARTESIAN_POINT('',(0.5,-8.75,-4.55181485540923));
#40483=CARTESIAN_POINT('',(0.,-8.25,-4.76313972081441));
#40484=CARTESIAN_POINT('',(0.,-8.25,-4.76313972081441));
#40485=CARTESIAN_POINT('',(0.5,-8.31698729810778,-5.30181485540923));
#40486=CARTESIAN_POINT('Origin',(0.,8.25,4.76313972081441));
#40487=CARTESIAN_POINT('',(0.5,8.75,4.55181485540922));
#40488=CARTESIAN_POINT('',(0.5,8.31698729810778,5.30181485540922));
#40489=CARTESIAN_POINT('',(0.5,8.75,4.55181485540922));
#40490=CARTESIAN_POINT('',(0.,8.25,4.76313972081441));
#40491=CARTESIAN_POINT('',(0.,8.25,4.76313972081441));
#40492=CARTESIAN_POINT('',(0.5,8.31698729810778,5.30181485540922));
#40493=CARTESIAN_POINT('Origin',(0.25,8.5,-2.52590742770462));
#40494=CARTESIAN_POINT('',(0.5,8.75,-2.52590742770462));
#40495=CARTESIAN_POINT('',(0.,8.25,-2.52590742770462));
#40496=CARTESIAN_POINT('Origin',(0.,-8.25,4.76313972081441));
#40497=CARTESIAN_POINT('',(0.5,-8.31698729810778,5.30181485540922));
#40498=CARTESIAN_POINT('',(0.5,-8.75,4.55181485540922));
#40499=CARTESIAN_POINT('',(0.5,-8.31698729810778,5.30181485540922));
#40500=CARTESIAN_POINT('',(0.,-8.25,4.76313972081441));
#40501=CARTESIAN_POINT('',(0.,-8.25,4.76313972081441));
#40502=CARTESIAN_POINT('',(0.5,-8.75,4.55181485540922));
#40503=CARTESIAN_POINT('Origin',(0.,-1.11022302462516E-15,9.52627944162883));
#40504=CARTESIAN_POINT('',(0.5,0.433012701892218,9.85362971081845));
#40505=CARTESIAN_POINT('',(0.5,-0.433012701892219,9.85362971081845));
#40506=CARTESIAN_POINT('',(0.5,0.433012701892219,9.85362971081845));
#40507=CARTESIAN_POINT('',(0.,2.77555756156289E-16,9.52627944162883));
#40508=CARTESIAN_POINT('',(0.,-1.11022302462516E-15,9.52627944162883));
#40509=CARTESIAN_POINT('',(0.5,-0.433012701892219,9.85362971081845));
#40510=CARTESIAN_POINT('Origin',(0.25,6.4375,6.09826221831542));
#40511=CARTESIAN_POINT('',(0.5,6.5625,6.31476856926153));
#40512=CARTESIAN_POINT('',(0.,6.3125,5.88175586736931));
#40513=CARTESIAN_POINT('Origin',(0.25,-2.0625,8.62416964602003));
#40514=CARTESIAN_POINT('',(0.5,-2.1875,8.84067599696614));
#40515=CARTESIAN_POINT('',(0.,-1.9375,8.40766329507393));
#40516=CARTESIAN_POINT('Origin',(0.,0.,9.85362971081845));
#40517=CARTESIAN_POINT('',(5.19749458287263,-0.43301270189222,9.85362971081845));
#40518=CARTESIAN_POINT('',(5.19749458287263,0.433012701892219,9.85362971081845));
#40519=CARTESIAN_POINT('Ctrl Pts',(5.19749458287264,-0.43301270189222,9.85362971081845));
#40520=CARTESIAN_POINT('Ctrl Pts',(5.20847043415501,1.38777878078145E-14,
9.85362971081845));
#40521=CARTESIAN_POINT('Ctrl Pts',(5.19749458287263,0.433012701892219,9.85362971081845));
#40522=CARTESIAN_POINT('',(0.,0.433012701892219,9.85362971081845));
#40523=CARTESIAN_POINT('',(0.,-0.433012701892219,9.85362971081845));
#40524=CARTESIAN_POINT('Origin',(0.25,-8.5,2.52590742770461));
#40525=CARTESIAN_POINT('',(0.5,-8.75,2.52590742770461));
#40526=CARTESIAN_POINT('',(0.,-8.25,2.52590742770461));
#40527=CARTESIAN_POINT('Origin',(0.,-8.53349364905389,4.92681485540922));
#40528=CARTESIAN_POINT('',(5.19749458287263,-8.75,4.55181485540923));
#40529=CARTESIAN_POINT('',(5.19749458287263,-8.31698729810778,5.30181485540922));
#40530=CARTESIAN_POINT('Ctrl Pts',(5.19749458287263,-8.75,4.55181485540923));
#40531=CARTESIAN_POINT('Ctrl Pts',(5.20847043415501,-8.53349364905388,4.92681485540924));
#40532=CARTESIAN_POINT('Ctrl Pts',(5.19749458287263,-8.31698729810778,5.30181485540922));
#40533=CARTESIAN_POINT('',(0.,-8.31698729810778,5.30181485540922));
#40534=CARTESIAN_POINT('',(0.,-8.75,4.55181485540922));
#40535=CARTESIAN_POINT('Origin',(0.,8.53349364905389,4.92681485540922));
#40536=CARTESIAN_POINT('',(5.19749458287264,8.31698729810778,5.30181485540922));
#40537=CARTESIAN_POINT('',(5.19749458287263,8.75,4.55181485540922));
#40538=CARTESIAN_POINT('Ctrl Pts',(5.19749458287264,8.31698729810778,5.30181485540922));
#40539=CARTESIAN_POINT('Ctrl Pts',(5.20847043415501,8.5334936490539,4.92681485540921));
#40540=CARTESIAN_POINT('Ctrl Pts',(5.19749458287263,8.75,4.55181485540922));
#40541=CARTESIAN_POINT('',(0.,8.75,4.55181485540922));
#40542=CARTESIAN_POINT('',(0.,8.31698729810778,5.30181485540922));
#40543=CARTESIAN_POINT('Origin',(0.25,-6.4375,-6.09826221831542));
#40544=CARTESIAN_POINT('',(0.5,-6.5625,-6.31476856926153));
#40545=CARTESIAN_POINT('',(0.,-6.3125,-5.88175586736931));
#40546=CARTESIAN_POINT('Origin',(0.,-8.53349364905389,-4.92681485540923));
#40547=CARTESIAN_POINT('',(5.19749458287263,-8.31698729810778,-5.30181485540923));
#40548=CARTESIAN_POINT('',(5.19749458287263,-8.75,-4.55181485540923));
#40549=CARTESIAN_POINT('Ctrl Pts',(5.19749458287263,-8.31698729810778,-5.30181485540923));
#40550=CARTESIAN_POINT('Ctrl Pts',(5.20847043415501,-8.5334936490539,-4.92681485540921));
#40551=CARTESIAN_POINT('Ctrl Pts',(5.19749458287263,-8.75,-4.55181485540923));
#40552=CARTESIAN_POINT('',(0.,-8.75,-4.55181485540923));
#40553=CARTESIAN_POINT('',(0.,-8.31698729810778,-5.30181485540923));
#40554=CARTESIAN_POINT('Origin',(0.,8.53349364905389,-4.92681485540923));
#40555=CARTESIAN_POINT('',(5.19749458287263,8.75,-4.55181485540923));
#40556=CARTESIAN_POINT('',(5.19749458287263,8.31698729810778,-5.30181485540923));
#40557=CARTESIAN_POINT('Ctrl Pts',(5.19749458287263,8.75,-4.55181485540923));
#40558=CARTESIAN_POINT('Ctrl Pts',(5.20847043415501,8.53349364905388,-4.92681485540924));
#40559=CARTESIAN_POINT('Ctrl Pts',(5.19749458287263,8.31698729810778,-5.30181485540923));
#40560=CARTESIAN_POINT('',(0.,8.31698729810778,-5.30181485540923));
#40561=CARTESIAN_POINT('',(0.,8.75,-4.55181485540923));
#40562=CARTESIAN_POINT('Origin',(0.25,2.0625,-8.62416964602004));
#40563=CARTESIAN_POINT('',(0.5,2.1875,-8.84067599696614));
#40564=CARTESIAN_POINT('',(0.,1.9375,-8.40766329507393));
#40565=CARTESIAN_POINT('Origin',(0.,-2.42861286636753E-15,-9.85362971081845));
#40566=CARTESIAN_POINT('',(5.19749458287263,0.433012701892218,-9.85362971081845));
#40567=CARTESIAN_POINT('',(5.19749458287263,-0.433012701892222,-9.85362971081845));
#40568=CARTESIAN_POINT('Ctrl Pts',(5.19749458287263,0.433012701892218,-9.85362971081845));
#40569=CARTESIAN_POINT('Ctrl Pts',(5.20847043415501,-1.65145674912992E-14,
-9.85362971081845));
#40570=CARTESIAN_POINT('Ctrl Pts',(5.19749458287263,-0.433012701892222,
-9.85362971081845));
#40571=CARTESIAN_POINT('',(0.,-0.433012701892222,-9.85362971081845));
#40572=CARTESIAN_POINT('',(0.,0.433012701892217,-9.85362971081845));
#40573=CARTESIAN_POINT('Origin',(0.,6.18668889256196E-16,10.1036297108185));
#40574=CARTESIAN_POINT('Ctrl Pts',(5.19749458287263,-8.31698729810778,5.30181485540922));
#40575=CARTESIAN_POINT('Ctrl Pts',(6.41034186570176,-4.375,7.57772228311384));
#40576=CARTESIAN_POINT('Ctrl Pts',(5.19749458287263,-0.43301270189222,9.85362971081845));
#40577=CARTESIAN_POINT('Origin',(0.,-8.75,5.05181485540922));
#40578=CARTESIAN_POINT('',(5.84018475750577,-8.75,-1.10351065767392E-15));
#40579=CARTESIAN_POINT('Ctrl Pts',(5.19749458287264,-8.75,-4.55181485540923));
#40580=CARTESIAN_POINT('Ctrl Pts',(5.84018475750577,-8.75,-2.13979915834902));
#40581=CARTESIAN_POINT('Ctrl Pts',(5.84018475750577,-8.75,-1.13545536609391E-15));
#40582=CARTESIAN_POINT('Ctrl Pts',(5.84018475750577,-8.75,-1.13545536609391E-15));
#40583=CARTESIAN_POINT('Ctrl Pts',(5.84018475750577,-8.75,2.13979915834902));
#40584=CARTESIAN_POINT('Ctrl Pts',(5.19749458287263,-8.75,4.55181485540923));
#40585=CARTESIAN_POINT('Origin',(0.,-8.75,-5.05181485540923));
#40586=CARTESIAN_POINT('Ctrl Pts',(5.19749458287263,-0.433012701892222,
-9.85362971081845));
#40587=CARTESIAN_POINT('Ctrl Pts',(6.41034186570176,-4.375,-7.57772228311384));
#40588=CARTESIAN_POINT('Ctrl Pts',(5.19749458287263,-8.31698729810778,-5.30181485540923));
#40589=CARTESIAN_POINT('Origin',(0.,0.,0.));
#40590=CARTESIAN_POINT('',(1.38777878078145E-16,-6.2,-7.59281015471359E-16));
#40591=CARTESIAN_POINT('Origin',(0.,0.,0.));
#40592=CARTESIAN_POINT('Origin',(5.75,-0.875,-3.24759526419165));
#40593=CARTESIAN_POINT('',(6.,-3.5,-2.02072594216369));
#40594=CARTESIAN_POINT('',(6.,-5.55111512312578E-16,-4.04145188432738));
#40595=CARTESIAN_POINT('',(6.,-1.,-3.46410161513775));
#40596=CARTESIAN_POINT('',(5.5,-6.36345143234944E-16,-3.46410161513775));
#40597=CARTESIAN_POINT('',(6.,-2.77555756156289E-16,-4.04145188432738));
#40598=CARTESIAN_POINT('',(5.5,-3.,-1.73205080756888));
#40599=CARTESIAN_POINT('',(5.5,-0.75,-3.03108891324554));
#40600=CARTESIAN_POINT('',(6.,-3.5,-2.02072594216369));
#40601=CARTESIAN_POINT('Origin',(5.75,2.375,-2.38156986040721));
#40602=CARTESIAN_POINT('',(6.,3.5,-2.02072594216369));
#40603=CARTESIAN_POINT('',(6.,2.5,-2.59807621135332));
#40604=CARTESIAN_POINT('',(5.5,3.,-1.73205080756888));
#40605=CARTESIAN_POINT('',(6.,3.5,-2.02072594216369));
#40606=CARTESIAN_POINT('',(5.5,2.25,-2.1650635094611));
#40607=CARTESIAN_POINT('Origin',(5.75,0.875,3.24759526419165));
#40608=CARTESIAN_POINT('',(6.,3.5,2.02072594216369));
#40609=CARTESIAN_POINT('',(6.,-5.55111512312578E-16,4.04145188432738));
#40610=CARTESIAN_POINT('',(6.,1.,3.46410161513775));
#40611=CARTESIAN_POINT('',(5.5,2.12115047744981E-16,3.46410161513775));
#40612=CARTESIAN_POINT('',(6.,-5.55111512312578E-16,4.04145188432738));
#40613=CARTESIAN_POINT('',(5.5,3.,1.73205080756888));
#40614=CARTESIAN_POINT('',(5.5,0.75,3.03108891324554));
#40615=CARTESIAN_POINT('',(5.5,3.,1.73205080756888));
#40616=CARTESIAN_POINT('Origin',(5.75,-2.375,2.38156986040721));
#40617=CARTESIAN_POINT('',(5.5,-3.,1.73205080756888));
#40618=CARTESIAN_POINT('',(5.5,-2.25,2.1650635094611));
#40619=CARTESIAN_POINT('',(6.,-3.5,2.02072594216369));
#40620=CARTESIAN_POINT('',(6.,-2.5,2.59807621135332));
#40621=CARTESIAN_POINT('',(6.,-3.5,2.02072594216369));
#40622=CARTESIAN_POINT('Origin',(5.75,3.25,0.866025403784438));
#40623=CARTESIAN_POINT('',(6.,3.5,0.866025403784438));
#40624=CARTESIAN_POINT('',(5.5,3.,0.866025403784438));
#40625=CARTESIAN_POINT('Origin',(5.75,-3.25,-0.866025403784439));
#40626=CARTESIAN_POINT('',(5.5,-3.,-0.866025403784439));
#40627=CARTESIAN_POINT('',(6.,-3.5,-0.866025403784439));
#40628=CARTESIAN_POINT('Origin',(6.,3.,-1.73205080756888));
#40629=CARTESIAN_POINT('',(2.,3.,-1.73205080756888));
#40630=CARTESIAN_POINT('',(6.,3.,-1.73205080756888));
#40631=CARTESIAN_POINT('',(2.,-5.55111512312578E-16,-3.46410161513775));
#40632=CARTESIAN_POINT('',(2.,-6.36345143234944E-16,-3.46410161513775));
#40633=CARTESIAN_POINT('',(6.,-6.36345143234944E-16,-3.46410161513775));
#40634=CARTESIAN_POINT('Origin',(6.,3.,1.73205080756888));
#40635=CARTESIAN_POINT('',(2.,3.,1.73205080756888));
#40636=CARTESIAN_POINT('',(6.,3.,1.73205080756888));
#40637=CARTESIAN_POINT('',(2.,3.,-1.73205080756888));
#40638=CARTESIAN_POINT('Origin',(6.,0.,3.46410161513775));
#40639=CARTESIAN_POINT('',(2.,0.,3.46410161513775));
#40640=CARTESIAN_POINT('',(6.,2.12115047744981E-16,3.46410161513775));
#40641=CARTESIAN_POINT('',(2.,3.,1.73205080756888));
#40642=CARTESIAN_POINT('Origin',(6.,0.,0.));
#40643=CARTESIAN_POINT('',(6.,-8.4732,-1.03766772585354E-15));
#40644=CARTESIAN_POINT('Origin',(6.,0.,0.));
#40645=CARTESIAN_POINT('Origin',(6.,-3.,1.73205080756888));
#40646=CARTESIAN_POINT('',(2.,-3.,1.73205080756888));
#40647=CARTESIAN_POINT('',(6.,-3.,1.73205080756888));
#40648=CARTESIAN_POINT('',(2.,2.12115047744981E-16,3.46410161513775));
#40649=CARTESIAN_POINT('Origin',(6.,-3.,-1.73205080756888));
#40650=CARTESIAN_POINT('',(2.,-3.,-1.73205080756888));
#40651=CARTESIAN_POINT('',(6.,-3.,-1.73205080756888));
#40652=CARTESIAN_POINT('',(2.,-3.,1.73205080756888));
#40653=CARTESIAN_POINT('Origin',(6.,-5.55111512312578E-16,-3.46410161513775));
#40654=CARTESIAN_POINT('',(2.,-3.,-1.73205080756888));
#40655=CARTESIAN_POINT('Origin',(2.,0.,0.));
#40656=CARTESIAN_POINT('Origin',(5.464896073903,0.,0.));
#40657=CARTESIAN_POINT('',(5.464896073903,-9.4,-1.15116799119851E-15));
#40658=CARTESIAN_POINT('Ctrl Pts',(5.19749458287263,8.31698729810778,-5.30181485540923));
#40659=CARTESIAN_POINT('Ctrl Pts',(6.41034186570176,4.375,-7.57772228311383));
#40660=CARTESIAN_POINT('Ctrl Pts',(5.19749458287263,0.43301270189222,-9.85362971081845));
#40661=CARTESIAN_POINT('Ctrl Pts',(5.19749458287263,8.75,4.55181485540922));
#40662=CARTESIAN_POINT('Ctrl Pts',(6.41034186570176,8.75,-6.10622663543836E-15));
#40663=CARTESIAN_POINT('Ctrl Pts',(5.19749458287263,8.75,-4.55181485540923));
#40664=CARTESIAN_POINT('Ctrl Pts',(5.19749458287263,0.433012701892218,9.85362971081845));
#40665=CARTESIAN_POINT('Ctrl Pts',(6.41034186570176,4.375,7.57772228311384));
#40666=CARTESIAN_POINT('Ctrl Pts',(5.19749458287264,8.31698729810778,5.30181485540922));
#40667=CARTESIAN_POINT('Origin',(0.,8.75,5.05181485540922));
#40668=CARTESIAN_POINT('Origin',(0.,8.75,-5.05181485540923));
#40669=CARTESIAN_POINT('Origin',(0.,-1.85600666776859E-15,-10.1036297108185));
#40670=CARTESIAN_POINT('Origin',(-11.,6.64,0.));
#40671=CARTESIAN_POINT('',(-11.,-6.64,-8.13165474633843E-16));
#40672=CARTESIAN_POINT('Origin',(-11.,0.,0.));
#40673=CARTESIAN_POINT('Origin',(-10.75,0.,0.));
#40674=CARTESIAN_POINT('',(-10.5,-7.14,-8.7439781459121E-16));
#40675=CARTESIAN_POINT('Origin',(-10.5,0.,0.));
#40676=CARTESIAN_POINT('',(-10.75,-6.89,-8.43781644612526E-16));
#40677=CARTESIAN_POINT('Origin',(-6.25,0.,0.));
#40678=CARTESIAN_POINT('',(-2.,-7.14,-8.7439781459121E-16));
#40679=CARTESIAN_POINT('Origin',(-2.,0.,0.));
#40680=CARTESIAN_POINT('',(-6.25,-7.14,-8.7439781459121E-16));
#40681=CARTESIAN_POINT('Origin',(-2.,6.2,0.));
#40682=CARTESIAN_POINT('',(-2.,-6.2,-7.59281015471359E-16));
#40683=CARTESIAN_POINT('Origin',(-2.,0.,0.));
#40684=CARTESIAN_POINT('Origin',(-1.,0.,0.));
#40685=CARTESIAN_POINT('',(-1.,-6.2,-7.59281015471359E-16));
#46375=UNCERTAINTY_MEASURE_WITH_UNIT(LENGTH_MEASURE(0.01),#46396,
'DISTANCE_ACCURACY_VALUE',
'Maximum model space distance between geometric entities at asserted c
onnectivities');
#46379=UNCERTAINTY_MEASURE_WITH_UNIT(LENGTH_MEASURE(0.01),#46396,
'DISTANCE_ACCURACY_VALUE',
'Maximum model space distance between geometric entities at asserted c
onnectivities');
#46391=(
GEOMETRIC_REPRESENTATION_CONTEXT(3)
GLOBAL_UNCERTAINTY_ASSIGNED_CONTEXT((#46375))
GLOBAL_UNIT_ASSIGNED_CONTEXT((#46396,#46398,#46399))
REPRESENTATION_CONTEXT('','3D')
);
#46395=(
GEOMETRIC_REPRESENTATION_CONTEXT(3)
GLOBAL_UNCERTAINTY_ASSIGNED_CONTEXT((#46379))
GLOBAL_UNIT_ASSIGNED_CONTEXT((#46396,#46398,#46399))
REPRESENTATION_CONTEXT('','3D')
);
#46396=(
LENGTH_UNIT()
NAMED_UNIT(*)
SI_UNIT(.MILLI.,.METRE.)
);
#46398=(
NAMED_UNIT(*)
PLANE_ANGLE_UNIT()
SI_UNIT($,.RADIAN.)
);
#46399=(
NAMED_UNIT(*)
SI_UNIT($,.STERADIAN.)
SOLID_ANGLE_UNIT()
);
#46411=SHAPE_DEFINITION_REPRESENTATION(#46426,#46466);
#46426=PRODUCT_DEFINITION_SHAPE('',$,#46482);
#46466=SHAPE_REPRESENTATION('',(#26528),#46391);
#46470=PRODUCT_DEFINITION_CONTEXT('part definition',#46517,'design');
#46482=PRODUCT_DEFINITION('2026-10-26-00-51-20-172',
'14_Case_Drain_Plug_9-16-18',#46497,#46470);
#46497=PRODUCT_DEFINITION_FORMATION('',$,#46530);
#46517=APPLICATION_CONTEXT(
'Core Data for Automotive Mechanical Design Process');
#46518=PRODUCT_CONTEXT('part definition',#46517,'mechanical');
#46530=PRODUCT('2026-10-26-00-51-20-172','14_Case_Drain_Plug_9-16-18',$,
(#46518));
#46583=COLOUR_RGB('Sky Blue',0.24,0.69,0.87);
#46584=FILL_AREA_STYLE_COLOUR('',#46583);
#46585=FILL_AREA_STYLE('',(#46584));
#46586=SURFACE_STYLE_FILL_AREA(#46585);
#46587=SURFACE_SIDE_STYLE('',(#46586));
#46588=SURFACE_STYLE_USAGE(.BOTH.,#46587);
#46589=PRESENTATION_STYLE_ASSIGNMENT((#46588));
ENDSEC;
END-ISO-10303-21;
